ISO-10303-21;
HEADER;
/* Generated by software containing ST-Developer
 * from STEP Tools, Inc. (www.steptools.com) 
 */

FILE_DESCRIPTION(
/* description */ ('Turntable on roller ring'),
/* implementation_level */ '2;1');

FILE_NAME(
/* name */ 'Retention collar.step',
/* time_stamp */ '2026-10-28T03:23:59-07:00',
/* author */ (''),
/* organization */ (''),
/* preprocessor_version */ 'ST-DEVELOPER v20.2',
/* originating_system */ 'Autodesk Translation Framework v15.17.0.0',
/* authorisation */ '');

FILE_SCHEMA (('AUTOMOTIVE_DESIGN { 1 0 10303 214 3 1 1 }'));
ENDSEC;

DATA;
#10=MECHANICAL_DESIGN_GEOMETRIC_PRESENTATION_REPRESENTATION('',(#639),#16281);
#417=B_SPLINE_CURVE_WITH_KNOTS('',3,(#14221,#14222,#14223,#14224,#14225,
#14226,#14227,#14228,#14229,#14230,#14231,#14232,#14233,#14234),
 .UNSPECIFIED.,.F.,.F.,(4,2,2,2,2,2,4),(0.714680326757343,0.792648662700719,
0.871912238073926,0.951175813447133,1.03043938882034,1.10970296419355,1.18767130013692),
 .UNSPECIFIED.);
#418=B_SPLINE_CURVE_WITH_KNOTS('',3,(#14237,#14238,#14239,#14240,#14241,
#14242,#14243,#14244,#14245,#14246,#14247,#14248,#14249,#14250),
 .UNSPECIFIED.,.F.,.F.,(4,2,2,2,2,2,4),(0.0805631177925872,0.158531453735963,
0.237795029109171,0.317058604482378,0.396322179855585,0.475585755228792,
0.553554091172168),.UNSPECIFIED.);
#419=B_SPLINE_CURVE_WITH_KNOTS('',3,(#14253,#14254,#14255,#14256,#14257,
#14258,#14259,#14260,#14261,#14262,#14263,#14264,#14265,#14266,#14267,#14268,
#14269,#14270,#14271,#14272,#14273,#14274,#14275,#14276,#14277,#14278,#14279,
#14280,#14281,#14282,#14283,#14284,#14285,#14286),.UNSPECIFIED.,.T.,.F.,
(4,2,2,2,2,2,2,2,2,2,2,2,2,2,2,2,4),(0.,0.0791819055472367,0.158363811094473,
0.237545215630595,0.316726620166717,0.395908024702839,0.475089429238961,
0.554271334786198,0.633453240333435,0.712635145880671,0.791817051427908,
0.87099845596403,0.950179860500152,1.02936126503627,1.1085426695724,1.18772457511963,
1.26690648066687),.UNSPECIFIED.);
#520=SHAPE_REPRESENTATION_RELATIONSHIP('SRR','None',#16536,#575);
#575=ADVANCED_BREP_SHAPE_REPRESENTATION('',(#710),#16230);
#639=STYLED_ITEM('',(#16925),#710);
#710=MANIFOLD_SOLID_BREP('Body1',#8381);
#861=FACE_BOUND('',#2037,.T.);
#862=FACE_BOUND('',#2039,.T.);
#863=FACE_BOUND('',#2041,.T.);
#864=FACE_BOUND('',#2043,.T.);
#1059=PLANE('',#9454);
#1060=PLANE('',#9459);
#1061=PLANE('',#9466);
#1062=PLANE('',#9467);
#1424=FACE_OUTER_BOUND('',#2033,.T.);
#1425=FACE_OUTER_BOUND('',#2034,.T.);
#1426=FACE_OUTER_BOUND('',#2035,.T.);
#1427=FACE_OUTER_BOUND('',#2036,.T.);
#1428=FACE_OUTER_BOUND('',#2038,.T.);
#1429=FACE_OUTER_BOUND('',#2040,.T.);
#1430=FACE_OUTER_BOUND('',#2042,.T.);
#2033=EDGE_LOOP('',(#6401,#6402,#6403));
#2034=EDGE_LOOP('',(#6404,#6405,#6406,#6407,#6408,#6409,#6410,#6411));
#2035=EDGE_LOOP('',(#6412,#6413));
#2036=EDGE_LOOP('',(#6414,#6415,#6416,#6417));
#2037=EDGE_LOOP('',(#6418,#6419,#6420,#6421));
#2038=EDGE_LOOP('',(#6422,#6423,#6424,#6425));
#2039=EDGE_LOOP('',(#6426));
#2040=EDGE_LOOP('',(#6427));
#2041=EDGE_LOOP('',(#6428));
#2042=EDGE_LOOP('',(#6429));
#2043=EDGE_LOOP('',(#6430));
#2636=LINE('',#14215,#3119);
#2637=LINE('',#14252,#3120);
#2638=LINE('',#14288,#3121);
#2639=LINE('',#14293,#3122);
#2640=LINE('',#14299,#3123);
#3119=VECTOR('',#11173,1.);
#3120=VECTOR('',#11182,0.21);
#3121=VECTOR('',#11185,1.);
#3122=VECTOR('',#11190,1.255);
#3123=VECTOR('',#11197,1.8);
#3676=CIRCLE('',#9455,0.21);
#3677=CIRCLE('',#9456,0.21);
#3678=CIRCLE('',#9458,0.21);
#3679=CIRCLE('',#9461,1.255);
#3680=CIRCLE('',#9462,1.255);
#3681=CIRCLE('',#9464,1.8);
#3682=CIRCLE('',#9465,1.8);
#4205=VERTEX_POINT('',#14213);
#4206=VERTEX_POINT('',#14214);
#4207=VERTEX_POINT('',#14216);
#4208=VERTEX_POINT('',#14220);
#4209=VERTEX_POINT('',#14235);
#4210=VERTEX_POINT('',#14251);
#4211=VERTEX_POINT('',#14290);
#4212=VERTEX_POINT('',#14292);
#4213=VERTEX_POINT('',#14296);
#4214=VERTEX_POINT('',#14298);
#5011=EDGE_CURVE('',#4205,#4206,#2636,.T.);
#5012=EDGE_CURVE('',#4205,#4207,#3676,.T.);
#5013=EDGE_CURVE('',#4207,#4206,#3677,.T.);
#5014=EDGE_CURVE('',#4208,#4205,#417,.T.);
#5015=EDGE_CURVE('',#4209,#4208,#3678,.T.);
#5016=EDGE_CURVE('',#4206,#4209,#418,.T.);
#5017=EDGE_CURVE('',#4207,#4210,#2637,.T.);
#5018=EDGE_CURVE('',#4210,#4210,#419,.T.);
#5019=EDGE_CURVE('',#4209,#4208,#2638,.T.);
#5020=EDGE_CURVE('',#4211,#4211,#3679,.T.);
#5021=EDGE_CURVE('',#4211,#4212,#2639,.T.);
#5022=EDGE_CURVE('',#4212,#4212,#3680,.T.);
#5023=EDGE_CURVE('',#4213,#4213,#3681,.T.);
#5024=EDGE_CURVE('',#4213,#4214,#2640,.T.);
#5025=EDGE_CURVE('',#4214,#4214,#3682,.T.);
#6401=ORIENTED_EDGE('',*,*,#5011,.F.);
#6402=ORIENTED_EDGE('',*,*,#5012,.T.);
#6403=ORIENTED_EDGE('',*,*,#5013,.T.);
#6404=ORIENTED_EDGE('',*,*,#5014,.F.);
#6405=ORIENTED_EDGE('',*,*,#5015,.F.);
#6406=ORIENTED_EDGE('',*,*,#5016,.F.);
#6407=ORIENTED_EDGE('',*,*,#5013,.F.);
#6408=ORIENTED_EDGE('',*,*,#5017,.T.);
#6409=ORIENTED_EDGE('',*,*,#5018,.F.);
#6410=ORIENTED_EDGE('',*,*,#5017,.F.);
#6411=ORIENTED_EDGE('',*,*,#5012,.F.);
#6412=ORIENTED_EDGE('',*,*,#5019,.F.);
#6413=ORIENTED_EDGE('',*,*,#5015,.T.);
#6414=ORIENTED_EDGE('',*,*,#5020,.F.);
#6415=ORIENTED_EDGE('',*,*,#5021,.T.);
#6416=ORIENTED_EDGE('',*,*,#5022,.T.);
#6417=ORIENTED_EDGE('',*,*,#5021,.F.);
#6418=ORIENTED_EDGE('',*,*,#5016,.T.);
#6419=ORIENTED_EDGE('',*,*,#5019,.T.);
#6420=ORIENTED_EDGE('',*,*,#5014,.T.);
#6421=ORIENTED_EDGE('',*,*,#5011,.T.);
#6422=ORIENTED_EDGE('',*,*,#5023,.F.);
#6423=ORIENTED_EDGE('',*,*,#5024,.T.);
#6424=ORIENTED_EDGE('',*,*,#5025,.T.);
#6425=ORIENTED_EDGE('',*,*,#5024,.F.);
#6426=ORIENTED_EDGE('',*,*,#5018,.T.);
#6427=ORIENTED_EDGE('',*,*,#5023,.T.);
#6428=ORIENTED_EDGE('',*,*,#5020,.T.);
#6429=ORIENTED_EDGE('',*,*,#5025,.F.);
#6430=ORIENTED_EDGE('',*,*,#5022,.F.);
#7747=CYLINDRICAL_SURFACE('',#9457,0.21);
#7748=CYLINDRICAL_SURFACE('',#9460,1.255);
#7749=CYLINDRICAL_SURFACE('',#9463,1.8);
#8027=ADVANCED_FACE('',(#1424),#1059,.T.);
#8028=ADVANCED_FACE('',(#1425),#7747,.F.);
#8029=ADVANCED_FACE('',(#1426),#1060,.T.);
#8030=ADVANCED_FACE('',(#1427,#861),#7748,.F.);
#8031=ADVANCED_FACE('',(#1428,#862),#7749,.T.);
#8032=ADVANCED_FACE('',(#1429,#863),#1061,.T.);
#8033=ADVANCED_FACE('',(#1430,#864),#1062,.F.);
#8381=CLOSED_SHELL('',(#8027,#8028,#8029,#8030,#8031,#8032,#8033));
#9453=AXIS2_PLACEMENT_3D('',#14211,#11169,#11170);
#9454=AXIS2_PLACEMENT_3D('',#14212,#11171,#11172);
#9455=AXIS2_PLACEMENT_3D('',#14217,#11174,#11175);
#9456=AXIS2_PLACEMENT_3D('',#14218,#11176,#11177);
#9457=AXIS2_PLACEMENT_3D('',#14219,#11178,#11179);
#9458=AXIS2_PLACEMENT_3D('',#14236,#11180,#11181);
#9459=AXIS2_PLACEMENT_3D('',#14287,#11183,#11184);
#9460=AXIS2_PLACEMENT_3D('',#14289,#11186,#11187);
#9461=AXIS2_PLACEMENT_3D('',#14291,#11188,#11189);
#9462=AXIS2_PLACEMENT_3D('',#14294,#11191,#11192);
#9463=AXIS2_PLACEMENT_3D('',#14295,#11193,#11194);
#9464=AXIS2_PLACEMENT_3D('',#14297,#11195,#11196);
#9465=AXIS2_PLACEMENT_3D('',#14300,#11198,#11199);
#9466=AXIS2_PLACEMENT_3D('',#14301,#11200,#11201);
#9467=AXIS2_PLACEMENT_3D('',#14302,#11202,#11203);
#11169=DIRECTION('axis',(0.,0.,1.));
#11170=DIRECTION('refdir',(1.,0.,0.));
#11171=DIRECTION('center_axis',(0.,1.,0.));
#11172=DIRECTION('ref_axis',(1.,0.,0.));
#11173=DIRECTION('',(0.,0.,1.));
#11174=DIRECTION('center_axis',(0.,1.,0.));
#11175=DIRECTION('ref_axis',(1.,0.,0.));
#11176=DIRECTION('center_axis',(0.,1.,0.));
#11177=DIRECTION('ref_axis',(1.,0.,0.));
#11178=DIRECTION('center_axis',(0.,1.,0.));
#11179=DIRECTION('ref_axis',(1.,0.,0.));
#11180=DIRECTION('center_axis',(0.,1.,0.));
#11181=DIRECTION('ref_axis',(1.,0.,0.));
#11182=DIRECTION('',(0.,1.,0.));
#11183=DIRECTION('center_axis',(0.,1.,0.));
#11184=DIRECTION('ref_axis',(1.,0.,0.));
#11185=DIRECTION('',(0.,0.,-1.));
#11186=DIRECTION('center_axis',(0.,0.,1.));
#11187=DIRECTION('ref_axis',(1.,0.,0.));
#11188=DIRECTION('center_axis',(0.,0.,-1.));
#11189=DIRECTION('ref_axis',(1.,0.,0.));
#11190=DIRECTION('',(0.,0.,-1.));
#11191=DIRECTION('center_axis',(0.,0.,-1.));
#11192=DIRECTION('ref_axis',(1.,0.,0.));
#11193=DIRECTION('center_axis',(0.,0.,1.));
#11194=DIRECTION('ref_axis',(1.,0.,0.));
#11195=DIRECTION('center_axis',(0.,0.,1.));
#11196=DIRECTION('ref_axis',(1.,0.,0.));
#11197=DIRECTION('',(0.,0.,-1.));
#11198=DIRECTION('center_axis',(0.,0.,1.));
#11199=DIRECTION('ref_axis',(1.,0.,0.));
#11200=DIRECTION('center_axis',(0.,0.,1.));
#11201=DIRECTION('ref_axis',(1.,0.,0.));
#11202=DIRECTION('center_axis',(0.,0.,1.));
#11203=DIRECTION('ref_axis',(1.,0.,0.));
#14211=CARTESIAN_POINT('',(0.,0.,0.));
#14212=CARTESIAN_POINT('Origin',(0.,1.24,2.4));
#14213=CARTESIAN_POINT('',(-0.193455421221531,1.24,2.31829932680816));
#14214=CARTESIAN_POINT('',(-0.193455421221531,1.24,2.48170067319184));
#14215=CARTESIAN_POINT('',(-0.193455421221531,1.24,2.));
#14216=CARTESIAN_POINT('',(-0.21,1.24,2.4));
#14217=CARTESIAN_POINT('Origin',(0.,1.24,2.4));
#14218=CARTESIAN_POINT('Origin',(0.,1.24,2.4));
#14219=CARTESIAN_POINT('Origin',(0.,1.24,2.4));
#14220=CARTESIAN_POINT('',(0.193455421221531,1.24,2.31829932680816));
#14221=CARTESIAN_POINT('Ctrl Pts',(0.19345542122153,1.24,2.31829932680816));
#14222=CARTESIAN_POINT('Ctrl Pts',(0.182741806873435,1.24167145707784,2.29293103184137));
#14223=CARTESIAN_POINT('Ctrl Pts',(0.16680484953796,1.24400210952839,2.26982000143961));
#14224=CARTESIAN_POINT('Ctrl Pts',(0.129875785635208,1.24840249136865,2.23289093753686));
#14225=CARTESIAN_POINT('Ctrl Pts',(0.106295060941802,1.2507589672592,2.2167372734261));
#14226=CARTESIAN_POINT('Ctrl Pts',(0.0545698089447938,1.25408084670822,
2.19529044194989));
#14227=CARTESIAN_POINT('Ctrl Pts',(0.0264211917910691,1.255,2.19));
#14228=CARTESIAN_POINT('Ctrl Pts',(-0.0264211917910689,1.255,2.19));
#14229=CARTESIAN_POINT('Ctrl Pts',(-0.0545698089447936,1.25408084670822,
2.19529044194989));
#14230=CARTESIAN_POINT('Ctrl Pts',(-0.106295060941802,1.2507589672592,2.2167372734261));
#14231=CARTESIAN_POINT('Ctrl Pts',(-0.129875785635207,1.24840249136865,
2.23289093753686));
#14232=CARTESIAN_POINT('Ctrl Pts',(-0.16680484953796,1.24400210952839,2.26982000143961));
#14233=CARTESIAN_POINT('Ctrl Pts',(-0.182741806873435,1.24167145707784,
2.29293103184137));
#14234=CARTESIAN_POINT('Ctrl Pts',(-0.193455421221531,1.24,2.31829932680816));
#14235=CARTESIAN_POINT('',(0.193455421221531,1.24,2.48170067319184));
#14236=CARTESIAN_POINT('Origin',(0.,1.24,2.4));
#14237=CARTESIAN_POINT('Ctrl Pts',(-0.193455421221531,1.24,2.48170067319184));
#14238=CARTESIAN_POINT('Ctrl Pts',(-0.182741806873435,1.24167145707784,
2.50706896815863));
#14239=CARTESIAN_POINT('Ctrl Pts',(-0.16680484953796,1.24400210952839,2.53017999856039));
#14240=CARTESIAN_POINT('Ctrl Pts',(-0.129875785635208,1.24840249136865,
2.56710906246314));
#14241=CARTESIAN_POINT('Ctrl Pts',(-0.106295060941802,1.2507589672592,2.5832627265739));
#14242=CARTESIAN_POINT('Ctrl Pts',(-0.0545698089447938,1.25408084670822,
2.6047095580501));
#14243=CARTESIAN_POINT('Ctrl Pts',(-0.0264211917910691,1.255,2.61));
#14244=CARTESIAN_POINT('Ctrl Pts',(0.026421191791069,1.255,2.61));
#14245=CARTESIAN_POINT('Ctrl Pts',(0.0545698089447936,1.25408084670822,
2.60470955805011));
#14246=CARTESIAN_POINT('Ctrl Pts',(0.106295060941802,1.2507589672592,2.5832627265739));
#14247=CARTESIAN_POINT('Ctrl Pts',(0.129875785635207,1.24840249136865,2.56710906246314));
#14248=CARTESIAN_POINT('Ctrl Pts',(0.16680484953796,1.24400210952839,2.53017999856039));
#14249=CARTESIAN_POINT('Ctrl Pts',(0.182741806873434,1.24167145707784,2.50706896815863));
#14250=CARTESIAN_POINT('Ctrl Pts',(0.19345542122153,1.24,2.48170067319184));
#14251=CARTESIAN_POINT('',(-0.21,1.78770802985275,2.4));
#14252=CARTESIAN_POINT('',(-0.21,1.24,2.4));
#14253=CARTESIAN_POINT('Ctrl Pts',(-0.21,1.78770802985275,2.4));
#14254=CARTESIAN_POINT('Ctrl Pts',(-0.21,1.78770802985275,2.37360603148425));
#14255=CARTESIAN_POINT('Ctrl Pts',(-0.204720232951726,1.78835284034214,
2.34546934556602));
#14256=CARTESIAN_POINT('Ctrl Pts',(-0.183281523978899,1.79067700538683,
2.29373688397397));
#14257=CARTESIAN_POINT('Ctrl Pts',(-0.167123888882363,1.79232226897314,
2.27013904078401));
#14258=CARTESIAN_POINT('Ctrl Pts',(-0.129861077103665,1.79540680803063,
2.23287622900532));
#14259=CARTESIAN_POINT('Ctrl Pts',(-0.106263182528071,1.79704717240673,
2.2167185016358));
#14260=CARTESIAN_POINT('Ctrl Pts',(-0.0545305475112074,1.79936011492601,
2.19527972468261));
#14261=CARTESIAN_POINT('Ctrl Pts',(-0.0263938015120406,1.8,2.19));
#14262=CARTESIAN_POINT('Ctrl Pts',(0.0263938015120407,1.8,2.19));
#14263=CARTESIAN_POINT('Ctrl Pts',(0.0545305475112074,1.79936011492601,
2.19527972468261));
#14264=CARTESIAN_POINT('Ctrl Pts',(0.106263182528071,1.79704717240673,2.2167185016358));
#14265=CARTESIAN_POINT('Ctrl Pts',(0.129861077103665,1.79540680803063,2.23287622900532));
#14266=CARTESIAN_POINT('Ctrl Pts',(0.167123888882363,1.79232226897314,2.27013904078401));
#14267=CARTESIAN_POINT('Ctrl Pts',(0.183281523978899,1.79067700538683,2.29373688397397));
#14268=CARTESIAN_POINT('Ctrl Pts',(0.204720232951726,1.78835284034214,2.34546934556602));
#14269=CARTESIAN_POINT('Ctrl Pts',(0.21,1.78770802985275,2.37360603148425));
#14270=CARTESIAN_POINT('Ctrl Pts',(0.21,1.78770802985275,2.42639396851575));
#14271=CARTESIAN_POINT('Ctrl Pts',(0.204720232951726,1.78835284034214,2.45453065443398));
#14272=CARTESIAN_POINT('Ctrl Pts',(0.183281523978899,1.79067700538683,2.50626311602603));
#14273=CARTESIAN_POINT('Ctrl Pts',(0.167123888882363,1.79232226897314,2.52986095921599));
#14274=CARTESIAN_POINT('Ctrl Pts',(0.129861077103665,1.79540680803063,2.56712377099468));
#14275=CARTESIAN_POINT('Ctrl Pts',(0.106263182528071,1.79704717240673,2.5832814983642));
#14276=CARTESIAN_POINT('Ctrl Pts',(0.0545305475112074,1.79936011492601,
2.60472027531739));
#14277=CARTESIAN_POINT('Ctrl Pts',(0.0263938015120407,1.8,2.61));
#14278=CARTESIAN_POINT('Ctrl Pts',(-0.0263938015120406,1.8,2.61));
#14279=CARTESIAN_POINT('Ctrl Pts',(-0.0545305475112074,1.79936011492601,
2.60472027531739));
#14280=CARTESIAN_POINT('Ctrl Pts',(-0.106263182528071,1.79704717240673,
2.5832814983642));
#14281=CARTESIAN_POINT('Ctrl Pts',(-0.129861077103665,1.79540680803063,
2.56712377099468));
#14282=CARTESIAN_POINT('Ctrl Pts',(-0.167123888882363,1.79232226897314,
2.52986095921599));
#14283=CARTESIAN_POINT('Ctrl Pts',(-0.183281523978899,1.79067700538683,
2.50626311602603));
#14284=CARTESIAN_POINT('Ctrl Pts',(-0.204720232951726,1.78835284034214,
2.45453065443398));
#14285=CARTESIAN_POINT('Ctrl Pts',(-0.21,1.78770802985275,2.42639396851575));
#14286=CARTESIAN_POINT('Ctrl Pts',(-0.21,1.78770802985275,2.4));
#14287=CARTESIAN_POINT('Origin',(0.,1.24,2.4));
#14288=CARTESIAN_POINT('',(0.193455421221531,1.24,2.));
#14289=CARTESIAN_POINT('Origin',(0.,0.,2.));
#14290=CARTESIAN_POINT('',(-1.255,-1.53693173292993E-16,2.75));
#14291=CARTESIAN_POINT('Origin',(0.,0.,2.75));
#14292=CARTESIAN_POINT('',(-1.255,-1.53693173292993E-16,2.));
#14293=CARTESIAN_POINT('',(-1.255,-1.53693173292993E-16,2.));
#14294=CARTESIAN_POINT('Origin',(0.,0.,2.));
#14295=CARTESIAN_POINT('Origin',(0.,0.,2.));
#14296=CARTESIAN_POINT('',(-1.8,-2.20436423846524E-16,2.75));
#14297=CARTESIAN_POINT('Origin',(0.,0.,2.75));
#14298=CARTESIAN_POINT('',(-1.8,-2.20436423846524E-16,2.));
#14299=CARTESIAN_POINT('',(-1.8,-2.20436423846524E-16,2.));
#14300=CARTESIAN_POINT('Origin',(0.,0.,2.));
#14301=CARTESIAN_POINT('Origin',(0.,0.,2.75));
#14302=CARTESIAN_POINT('Origin',(0.,0.,2.));
#16161=UNCERTAINTY_MEASURE_WITH_UNIT(LENGTH_MEASURE(0.001),#16282,
'DISTANCE_ACCURACY_VALUE',
'Maximum model space distance between geometric entities at asserted c
onnectivities');
#16212=UNCERTAINTY_MEASURE_WITH_UNIT(LENGTH_MEASURE(0.001),#16282,
'DISTANCE_ACCURACY_VALUE',
'Maximum model space distance between geometric entities at asserted c
onnectivities');
#16230=(
GEOMETRIC_REPRESENTATION_CONTEXT(3)
GLOBAL_UNCERTAINTY_ASSIGNED_CONTEXT((#16161))
GLOBAL_UNIT_ASSIGNED_CONTEXT((#16282,#16284,#16285))
REPRESENTATION_CONTEXT('','3D')
);
#16281=(
GEOMETRIC_REPRESENTATION_CONTEXT(3)
GLOBAL_UNCERTAINTY_ASSIGNED_CONTEXT((#16212))
GLOBAL_UNIT_ASSIGNED_CONTEXT((#16282,#16284,#16285))
REPRESENTATION_CONTEXT('','3D')
);
#16282=(
LENGTH_UNIT()
NAMED_UNIT(*)
SI_UNIT(.CENTI.,.METRE.)
);
#16284=(
NAMED_UNIT(*)
PLANE_ANGLE_UNIT()
SI_UNIT($,.RADIAN.)
);
#16285=(
NAMED_UNIT(*)
SI_UNIT($,.STERADIAN.)
SOLID_ANGLE_UNIT()
);
#16303=SHAPE_DEFINITION_REPRESENTATION(#16376,#16536);
#16376=PRODUCT_DEFINITION_SHAPE('',$,#16605);
#16536=SHAPE_REPRESENTATION('',(#9453),#16230);
#16587=PRODUCT_DEFINITION_CONTEXT('part definition',#16793,'design');
#16605=PRODUCT_DEFINITION('Retention collar','Retention collar',#16673,
#16587);
#16673=PRODUCT_DEFINITION_FORMATION('',$,#16812);
#16793=APPLICATION_CONTEXT(
'Core Data for Automotive Mechanical Design Process');
#16794=PRODUCT_CONTEXT('part definition',#16793,'mechanical');
#16812=PRODUCT('Retention collar','Retention collar','Retention collar',
(#16794));
#16919=COLOUR_RGB('Sky Blue',0.24,0.69,0.87);
#16920=FILL_AREA_STYLE_COLOUR('',#16919);
#16921=FILL_AREA_STYLE('',(#16920));
#16922=SURFACE_STYLE_FILL_AREA(#16921);
#16923=SURFACE_SIDE_STYLE('',(#16922));
#16924=SURFACE_STYLE_USAGE(.BOTH.,#16923);
#16925=PRESENTATION_STYLE_ASSIGNMENT((#16924));
ENDSEC;
END-ISO-10303-21;
